ISO-10303-21;
HEADER;
/* Generated by software containing ST-Developer
 * from STEP Tools, Inc. (www.steptools.com) 
 */

FILE_DESCRIPTION(
/* description */ (''),
/* implementation_level */ '2;1');

FILE_NAME(
/* name */ '12_Check_Ball_D16_TPEE.step',
/* time_stamp */ '2026-10-26T06:13:19-07:00',
/* author */ (''),
/* organization */ (''),
/* preprocessor_version */ 'ST-DEVELOPER v20.2',
/* originating_system */ 'Autodesk Translation Framework v15.15.0.0',
/* authorisation */ '');

FILE_SCHEMA (('AUTOMOTIVE_DESIGN { 1 0 10303 214 3 1 1 }','TECHNICAL_DATA_PACKAGING'));
ENDSEC;

DATA;
#10=MECHANICAL_DESIGN_GEOMETRIC_PRESENTATION_REPRESENTATION('',(#310),#56639);
#243=SPHERICAL_SURFACE('',#18203,8.);
#270=SHAPE_REPRESENTATION_RELATIONSHIP('SRR','None',#56758,#290);
#290=ADVANCED_BREP_SHAPE_REPRESENTATION('',(#330),#56632);
#310=STYLED_ITEM('',(#56908),#330);
#330=MANIFOLD_SOLID_BREP('Body1',#16962);
#1125=CIRCLE('',#18204,8.);
#2345=FACE_OUTER_BOUND('',#3449,.T.);
#3449=EDGE_LOOP('',(#13342,#13343));
#7519=VERTEX_POINT('',#36430);
#7520=VERTEX_POINT('',#36431);
#9578=EDGE_CURVE('',#7519,#7520,#1125,.T.);
#13342=ORIENTED_EDGE('',*,*,#9578,.T.);
#13343=ORIENTED_EDGE('',*,*,#9578,.F.);
#16516=ADVANCED_FACE('',(#2345),#243,.T.);
#16962=CLOSED_SHELL('',(#16516));
#18202=AXIS2_PLACEMENT_3D('',#36428,#21333,#21334);
#18203=AXIS2_PLACEMENT_3D('',#36429,#21335,#21336);
#18204=AXIS2_PLACEMENT_3D('',#36432,#21337,#21338);
#21333=DIRECTION('axis',(0.,0.,1.));
#21334=DIRECTION('refdir',(1.,0.,0.));
#21335=DIRECTION('center_axis',(6.12323399573677E-17,0.,1.));
#21336=DIRECTION('ref_axis',(1.,0.,0.));
#21337=DIRECTION('center_axis',(1.22464679914735E-16,-1.,0.));
#21338=DIRECTION('ref_axis',(-1.,-1.22464679914735E-16,0.));
#36428=CARTESIAN_POINT('',(0.,0.,0.));
#36429=CARTESIAN_POINT('Origin',(0.,0.,0.));
#36430=CARTESIAN_POINT('',(-4.89858719658941E-16,-5.99903913064743E-32,
8.));
#36431=CARTESIAN_POINT('',(-4.89858719658941E-16,-5.99903913064743E-32,
-8.));
#36432=CARTESIAN_POINT('Origin',(0.,0.,0.));
#56610=UNCERTAINTY_MEASURE_WITH_UNIT(LENGTH_MEASURE(0.01),#56640,
'DISTANCE_ACCURACY_VALUE',
'Maximum model space distance between geometric entities at asserted c
onnectivities');
#56617=UNCERTAINTY_MEASURE_WITH_UNIT(LENGTH_MEASURE(0.01),#56640,
'DISTANCE_ACCURACY_VALUE',
'Maximum model space distance between geometric entities at asserted c
onnectivities');
#56632=(
GEOMETRIC_REPRESENTATION_CONTEXT(3)
GLOBAL_UNCERTAINTY_ASSIGNED_CONTEXT((#56610))
GLOBAL_UNIT_ASSIGNED_CONTEXT((#56640,#56642,#56643))
REPRESENTATION_CONTEXT('','3D')
);
#56639=(
GEOMETRIC_REPRESENTATION_CONTEXT(3)
GLOBAL_UNCERTAINTY_ASSIGNED_CONTEXT((#56617))
GLOBAL_UNIT_ASSIGNED_CONTEXT((#56640,#56642,#56643))
REPRESENTATION_CONTEXT('','3D')
);
#56640=(
LENGTH_UNIT()
NAMED_UNIT(*)
SI_UNIT(.MILLI.,.METRE.)
);
#56642=(
NAMED_UNIT(*)
PLANE_ANGLE_UNIT()
SI_UNIT($,.RADIAN.)
);
#56643=(
NAMED_UNIT(*)
SI_UNIT($,.STERADIAN.)
SOLID_ANGLE_UNIT()
);
#56658=SHAPE_DEFINITION_REPRESENTATION(#56679,#56758);
#56679=PRODUCT_DEFINITION_SHAPE('',$,#56780);
#56758=SHAPE_REPRESENTATION('',(#18202),#56632);
#56765=PRODUCT_DEFINITION_CONTEXT('part definition',#56830,'design');
#56780=PRODUCT_DEFINITION('2026-10-26-00-02-50-076',
'12_Check_Ball_D16_TPEE',#56801,#56765);
#56801=PRODUCT_DEFINITION_FORMATION('',$,#56846);
#56830=APPLICATION_CONTEXT(
'Core Data for Automotive Mechanical Design Process');
#56831=PRODUCT_CONTEXT('part definition',#56830,'mechanical');
#56846=PRODUCT('2026-10-26-00-02-50-076','12_Check_Ball_D16_TPEE',$,(#56831));
#56902=COLOUR_RGB('Sky Blue',0.24,0.69,0.87);
#56903=FILL_AREA_STYLE_COLOUR('',#56902);
#56904=FILL_AREA_STYLE('',(#56903));
#56905=SURFACE_STYLE_FILL_AREA(#56904);
#56906=SURFACE_SIDE_STYLE('',(#56905));
#56907=SURFACE_STYLE_USAGE(.BOTH.,#56906);
#56908=PRESENTATION_STYLE_ASSIGNMENT((#56907));
ENDSEC;
END-ISO-10303-21;
